ISO-10303-21;
HEADER;
/* Generated by software containing ST-Developer
 * from STEP Tools, Inc. (www.steptools.com) 
 */

FILE_DESCRIPTION(
/* description */ ('STEP AP214'),
/* implementation_level */ '2;1');

FILE_NAME(
/* name */ 'Ball Screw Spacer 1.step',
/* time_stamp */ '2026-11-15T14:49:54-08:00',
/* author */ (''),
/* organization */ (''),
/* preprocessor_version */ 'ST-DEVELOPER v20.2',
/* originating_system */ 'Autodesk Translation Framework v15.17.0.0',
/* authorisation */ '');

FILE_SCHEMA (('AUTOMOTIVE_DESIGN { 1 0 10303 214 3 1 1 }'));
ENDSEC;

DATA;
#10=MECHANICAL_DESIGN_GEOMETRIC_PRESENTATION_REPRESENTATION('',(#1114),#66721);
#1052=SHAPE_REPRESENTATION_RELATIONSHIP('SRR','None',#66913,#1083);
#1083=ADVANCED_BREP_SHAPE_REPRESENTATION('',(#1149),#66704);
#1114=STYLED_ITEM('',(#67095),#1149);
#1149=MANIFOLD_SOLID_BREP('Body1',#25680);
#1381=FACE_BOUND('',#4770,.T.);
#1382=FACE_BOUND('',#4771,.T.);
#1383=FACE_BOUND('',#4772,.T.);
#1384=FACE_BOUND('',#4773,.T.);
#1385=FACE_BOUND('',#4774,.T.);
#1386=FACE_BOUND('',#4775,.T.);
#1387=FACE_BOUND('',#4781,.T.);
#1388=FACE_BOUND('',#4782,.T.);
#1389=FACE_BOUND('',#4783,.T.);
#1390=FACE_BOUND('',#4784,.T.);
#1391=FACE_BOUND('',#4785,.T.);
#1392=FACE_BOUND('',#4786,.T.);
#2004=PLANE('',#27700);
#2005=PLANE('',#27701);
#2006=PLANE('',#27702);
#2007=PLANE('',#27703);
#2008=PLANE('',#27704);
#2009=PLANE('',#27705);
#2010=PLANE('',#27706);
#2011=PLANE('',#27707);
#2012=PLANE('',#27708);
#2013=PLANE('',#27709);
#2014=PLANE('',#27710);
#2015=PLANE('',#27711);
#3102=FACE_OUTER_BOUND('',#4757,.T.);
#3103=FACE_OUTER_BOUND('',#4758,.T.);
#3104=FACE_OUTER_BOUND('',#4759,.T.);
#3105=FACE_OUTER_BOUND('',#4760,.T.);
#3106=FACE_OUTER_BOUND('',#4761,.T.);
#3107=FACE_OUTER_BOUND('',#4762,.T.);
#3108=FACE_OUTER_BOUND('',#4763,.T.);
#3109=FACE_OUTER_BOUND('',#4764,.T.);
#3110=FACE_OUTER_BOUND('',#4765,.T.);
#3111=FACE_OUTER_BOUND('',#4766,.T.);
#3112=FACE_OUTER_BOUND('',#4767,.T.);
#3113=FACE_OUTER_BOUND('',#4768,.T.);
#3114=FACE_OUTER_BOUND('',#4769,.T.);
#3115=FACE_OUTER_BOUND('',#4776,.T.);
#3116=FACE_OUTER_BOUND('',#4777,.T.);
#3117=FACE_OUTER_BOUND('',#4778,.T.);
#3118=FACE_OUTER_BOUND('',#4779,.T.);
#3119=FACE_OUTER_BOUND('',#4780,.T.);
#4757=EDGE_LOOP('',(#20976,#20977,#20978,#20979));
#4758=EDGE_LOOP('',(#20980,#20981,#20982,#20983));
#4759=EDGE_LOOP('',(#20984,#20985,#20986,#20987));
#4760=EDGE_LOOP('',(#20988,#20989,#20990,#20991));
#4761=EDGE_LOOP('',(#20992,#20993,#20994,#20995));
#4762=EDGE_LOOP('',(#20996,#20997,#20998,#20999));
#4763=EDGE_LOOP('',(#21000,#21001,#21002,#21003));
#4764=EDGE_LOOP('',(#21004,#21005,#21006,#21007,#21008,#21009));
#4765=EDGE_LOOP('',(#21010,#21011,#21012,#21013,#21014,#21015));
#4766=EDGE_LOOP('',(#21016,#21017,#21018,#21019,#21020,#21021));
#4767=EDGE_LOOP('',(#21022,#21023,#21024,#21025,#21026,#21027));
#4768=EDGE_LOOP('',(#21028,#21029,#21030,#21031));
#4769=EDGE_LOOP('',(#21032,#21033,#21034,#21035));
#4770=EDGE_LOOP('',(#21036));
#4771=EDGE_LOOP('',(#21037));
#4772=EDGE_LOOP('',(#21038));
#4773=EDGE_LOOP('',(#21039));
#4774=EDGE_LOOP('',(#21040));
#4775=EDGE_LOOP('',(#21041));
#4776=EDGE_LOOP('',(#21042,#21043,#21044,#21045));
#4777=EDGE_LOOP('',(#21046,#21047,#21048,#21049));
#4778=EDGE_LOOP('',(#21050,#21051,#21052,#21053));
#4779=EDGE_LOOP('',(#21054,#21055,#21056,#21057));
#4780=EDGE_LOOP('',(#21058,#21059,#21060,#21061,#21062,#21063,#21064,#21065));
#4781=EDGE_LOOP('',(#21066));
#4782=EDGE_LOOP('',(#21067));
#4783=EDGE_LOOP('',(#21068));
#4784=EDGE_LOOP('',(#21069));
#4785=EDGE_LOOP('',(#21070));
#4786=EDGE_LOOP('',(#21071));
#6856=LINE('',#41134,#8845);
#6857=LINE('',#41140,#8846);
#6858=LINE('',#41146,#8847);
#6859=LINE('',#41152,#8848);
#6860=LINE('',#41158,#8849);
#6861=LINE('',#41164,#8850);
#6862=LINE('',#41169,#8851);
#6863=LINE('',#41171,#8852);
#6864=LINE('',#41173,#8853);
#6865=LINE('',#41174,#8854);
#6866=LINE('',#41177,#8855);
#6867=LINE('',#41179,#8856);
#6868=LINE('',#41181,#8857);
#6869=LINE('',#41183,#8858);
#6870=LINE('',#41184,#8859);
#6871=LINE('',#41188,#8860);
#6872=LINE('',#41189,#8861);
#6873=LINE('',#41191,#8862);
#6874=LINE('',#41192,#8863);
#6875=LINE('',#41196,#8864);
#6876=LINE('',#41198,#8865);
#6877=LINE('',#41199,#8866);
#6878=LINE('',#41201,#8867);
#6879=LINE('',#41202,#8868);
#6880=LINE('',#41205,#8869);
#6881=LINE('',#41207,#8870);
#6882=LINE('',#41208,#8871);
#6883=LINE('',#41209,#8872);
#6884=LINE('',#41212,#8873);
#6885=LINE('',#41213,#8874);
#6886=LINE('',#41217,#8875);
#6887=LINE('',#41218,#8876);
#6888=LINE('',#41220,#8877);
#6889=LINE('',#41223,#8878);
#6890=LINE('',#41224,#8879);
#6891=LINE('',#41226,#8880);
#8845=VECTOR('',#33415,3.);
#8846=VECTOR('',#33422,3.);
#8847=VECTOR('',#33429,3.25);
#8848=VECTOR('',#33436,3.25);
#8849=VECTOR('',#33443,3.25);
#8850=VECTOR('',#33450,3.25);
#8851=VECTOR('',#33455,1000.);
#8852=VECTOR('',#33456,1000.);
#8853=VECTOR('',#33457,1000.);
#8854=VECTOR('',#33458,1000.);
#8855=VECTOR('',#33461,1000.);
#8856=VECTOR('',#33462,1000.);
#8857=VECTOR('',#33463,1000.);
#8858=VECTOR('',#33464,1000.);
#8859=VECTOR('',#33465,1000.);
#8860=VECTOR('',#33468,1000.);
#8861=VECTOR('',#33469,1000.);
#8862=VECTOR('',#33470,1000.);
#8863=VECTOR('',#33471,1000.);
#8864=VECTOR('',#33474,1000.);
#8865=VECTOR('',#33475,1000.);
#8866=VECTOR('',#33476,1000.);
#8867=VECTOR('',#33477,1000.);
#8868=VECTOR('',#33478,1000.);
#8869=VECTOR('',#33481,1000.);
#8870=VECTOR('',#33482,1000.);
#8871=VECTOR('',#33483,1000.);
#8872=VECTOR('',#33484,1000.);
#8873=VECTOR('',#33487,1000.);
#8874=VECTOR('',#33488,1000.);
#8875=VECTOR('',#33493,1000.);
#8876=VECTOR('',#33494,1000.);
#8877=VECTOR('',#33497,1000.);
#8878=VECTOR('',#33500,1000.);
#8879=VECTOR('',#33501,1000.);
#8880=VECTOR('',#33504,1000.);
#10151=CIRCLE('',#27683,3.);
#10152=CIRCLE('',#27684,3.);
#10153=CIRCLE('',#27686,3.);
#10154=CIRCLE('',#27687,3.);
#10155=CIRCLE('',#27689,3.25);
#10156=CIRCLE('',#27690,3.25);
#10157=CIRCLE('',#27692,3.25);
#10158=CIRCLE('',#27693,3.25);
#10159=CIRCLE('',#27695,3.25);
#10160=CIRCLE('',#27696,3.25);
#10161=CIRCLE('',#27698,3.25);
#10162=CIRCLE('',#27699,3.25);
#12087=VERTEX_POINT('',#41131);
#12088=VERTEX_POINT('',#41133);
#12089=VERTEX_POINT('',#41137);
#12090=VERTEX_POINT('',#41139);
#12091=VERTEX_POINT('',#41143);
#12092=VERTEX_POINT('',#41145);
#12093=VERTEX_POINT('',#41149);
#12094=VERTEX_POINT('',#41151);
#12095=VERTEX_POINT('',#41155);
#12096=VERTEX_POINT('',#41157);
#12097=VERTEX_POINT('',#41161);
#12098=VERTEX_POINT('',#41163);
#12099=VERTEX_POINT('',#41167);
#12100=VERTEX_POINT('',#41168);
#12101=VERTEX_POINT('',#41170);
#12102=VERTEX_POINT('',#41172);
#12103=VERTEX_POINT('',#41176);
#12104=VERTEX_POINT('',#41178);
#12105=VERTEX_POINT('',#41180);
#12106=VERTEX_POINT('',#41182);
#12107=VERTEX_POINT('',#41186);
#12108=VERTEX_POINT('',#41187);
#12109=VERTEX_POINT('',#41190);
#12110=VERTEX_POINT('',#41194);
#12111=VERTEX_POINT('',#41195);
#12112=VERTEX_POINT('',#41197);
#12113=VERTEX_POINT('',#41200);
#12114=VERTEX_POINT('',#41204);
#12115=VERTEX_POINT('',#41206);
#12116=VERTEX_POINT('',#41211);
#12117=VERTEX_POINT('',#41216);
#12118=VERTEX_POINT('',#41222);
#15181=EDGE_CURVE('',#12087,#12087,#10151,.T.);
#15182=EDGE_CURVE('',#12087,#12088,#6856,.T.);
#15183=EDGE_CURVE('',#12088,#12088,#10152,.T.);
#15184=EDGE_CURVE('',#12089,#12089,#10153,.T.);
#15185=EDGE_CURVE('',#12089,#12090,#6857,.T.);
#15186=EDGE_CURVE('',#12090,#12090,#10154,.T.);
#15187=EDGE_CURVE('',#12091,#12091,#10155,.T.);
#15188=EDGE_CURVE('',#12091,#12092,#6858,.T.);
#15189=EDGE_CURVE('',#12092,#12092,#10156,.T.);
#15190=EDGE_CURVE('',#12093,#12093,#10157,.T.);
#15191=EDGE_CURVE('',#12093,#12094,#6859,.T.);
#15192=EDGE_CURVE('',#12094,#12094,#10158,.T.);
#15193=EDGE_CURVE('',#12095,#12095,#10159,.T.);
#15194=EDGE_CURVE('',#12095,#12096,#6860,.T.);
#15195=EDGE_CURVE('',#12096,#12096,#10160,.T.);
#15196=EDGE_CURVE('',#12097,#12097,#10161,.T.);
#15197=EDGE_CURVE('',#12097,#12098,#6861,.T.);
#15198=EDGE_CURVE('',#12098,#12098,#10162,.T.);
#15199=EDGE_CURVE('',#12099,#12100,#6862,.T.);
#15200=EDGE_CURVE('',#12101,#12099,#6863,.T.);
#15201=EDGE_CURVE('',#12101,#12102,#6864,.T.);
#15202=EDGE_CURVE('',#12102,#12100,#6865,.T.);
#15203=EDGE_CURVE('',#12103,#12101,#6866,.T.);
#15204=EDGE_CURVE('',#12104,#12103,#6867,.T.);
#15205=EDGE_CURVE('',#12104,#12105,#6868,.T.);
#15206=EDGE_CURVE('',#12105,#12106,#6869,.T.);
#15207=EDGE_CURVE('',#12102,#12106,#6870,.T.);
#15208=EDGE_CURVE('',#12107,#12108,#6871,.T.);
#15209=EDGE_CURVE('',#12107,#12100,#6872,.T.);
#15210=EDGE_CURVE('',#12106,#12109,#6873,.T.);
#15211=EDGE_CURVE('',#12108,#12109,#6874,.T.);
#15212=EDGE_CURVE('',#12110,#12111,#6875,.T.);
#15213=EDGE_CURVE('',#12112,#12110,#6876,.T.);
#15214=EDGE_CURVE('',#12108,#12112,#6877,.T.);
#15215=EDGE_CURVE('',#12109,#12113,#6878,.T.);
#15216=EDGE_CURVE('',#12111,#12113,#6879,.T.);
#15217=EDGE_CURVE('',#12114,#12104,#6880,.T.);
#15218=EDGE_CURVE('',#12114,#12115,#6881,.T.);
#15219=EDGE_CURVE('',#12111,#12115,#6882,.T.);
#15220=EDGE_CURVE('',#12113,#12105,#6883,.T.);
#15221=EDGE_CURVE('',#12116,#12115,#6884,.T.);
#15222=EDGE_CURVE('',#12110,#12116,#6885,.T.);
#15223=EDGE_CURVE('',#12117,#12107,#6886,.T.);
#15224=EDGE_CURVE('',#12117,#12099,#6887,.T.);
#15225=EDGE_CURVE('',#12103,#12117,#6888,.T.);
#15226=EDGE_CURVE('',#12118,#12114,#6889,.T.);
#15227=EDGE_CURVE('',#12118,#12116,#6890,.T.);
#15228=EDGE_CURVE('',#12112,#12118,#6891,.T.);
#20976=ORIENTED_EDGE('',*,*,#15181,.F.);
#20977=ORIENTED_EDGE('',*,*,#15182,.T.);
#20978=ORIENTED_EDGE('',*,*,#15183,.T.);
#20979=ORIENTED_EDGE('',*,*,#15182,.F.);
#20980=ORIENTED_EDGE('',*,*,#15184,.F.);
#20981=ORIENTED_EDGE('',*,*,#15185,.T.);
#20982=ORIENTED_EDGE('',*,*,#15186,.T.);
#20983=ORIENTED_EDGE('',*,*,#15185,.F.);
#20984=ORIENTED_EDGE('',*,*,#15187,.F.);
#20985=ORIENTED_EDGE('',*,*,#15188,.T.);
#20986=ORIENTED_EDGE('',*,*,#15189,.T.);
#20987=ORIENTED_EDGE('',*,*,#15188,.F.);
#20988=ORIENTED_EDGE('',*,*,#15190,.F.);
#20989=ORIENTED_EDGE('',*,*,#15191,.T.);
#20990=ORIENTED_EDGE('',*,*,#15192,.T.);
#20991=ORIENTED_EDGE('',*,*,#15191,.F.);
#20992=ORIENTED_EDGE('',*,*,#15193,.F.);
#20993=ORIENTED_EDGE('',*,*,#15194,.T.);
#20994=ORIENTED_EDGE('',*,*,#15195,.T.);
#20995=ORIENTED_EDGE('',*,*,#15194,.F.);
#20996=ORIENTED_EDGE('',*,*,#15196,.F.);
#20997=ORIENTED_EDGE('',*,*,#15197,.T.);
#20998=ORIENTED_EDGE('',*,*,#15198,.T.);
#20999=ORIENTED_EDGE('',*,*,#15197,.F.);
#21000=ORIENTED_EDGE('',*,*,#15199,.F.);
#21001=ORIENTED_EDGE('',*,*,#15200,.F.);
#21002=ORIENTED_EDGE('',*,*,#15201,.T.);
#21003=ORIENTED_EDGE('',*,*,#15202,.T.);
#21004=ORIENTED_EDGE('',*,*,#15201,.F.);
#21005=ORIENTED_EDGE('',*,*,#15203,.F.);
#21006=ORIENTED_EDGE('',*,*,#15204,.F.);
#21007=ORIENTED_EDGE('',*,*,#15205,.T.);
#21008=ORIENTED_EDGE('',*,*,#15206,.T.);
#21009=ORIENTED_EDGE('',*,*,#15207,.F.);
#21010=ORIENTED_EDGE('',*,*,#15208,.F.);
#21011=ORIENTED_EDGE('',*,*,#15209,.T.);
#21012=ORIENTED_EDGE('',*,*,#15202,.F.);
#21013=ORIENTED_EDGE('',*,*,#15207,.T.);
#21014=ORIENTED_EDGE('',*,*,#15210,.T.);
#21015=ORIENTED_EDGE('',*,*,#15211,.F.);
#21016=ORIENTED_EDGE('',*,*,#15212,.F.);
#21017=ORIENTED_EDGE('',*,*,#15213,.F.);
#21018=ORIENTED_EDGE('',*,*,#15214,.F.);
#21019=ORIENTED_EDGE('',*,*,#15211,.T.);
#21020=ORIENTED_EDGE('',*,*,#15215,.T.);
#21021=ORIENTED_EDGE('',*,*,#15216,.F.);
#21022=ORIENTED_EDGE('',*,*,#15217,.F.);
#21023=ORIENTED_EDGE('',*,*,#15218,.T.);
#21024=ORIENTED_EDGE('',*,*,#15219,.F.);
#21025=ORIENTED_EDGE('',*,*,#15216,.T.);
#21026=ORIENTED_EDGE('',*,*,#15220,.T.);
#21027=ORIENTED_EDGE('',*,*,#15205,.F.);
#21028=ORIENTED_EDGE('',*,*,#15221,.F.);
#21029=ORIENTED_EDGE('',*,*,#15222,.F.);
#21030=ORIENTED_EDGE('',*,*,#15212,.T.);
#21031=ORIENTED_EDGE('',*,*,#15219,.T.);
#21032=ORIENTED_EDGE('',*,*,#15206,.F.);
#21033=ORIENTED_EDGE('',*,*,#15220,.F.);
#21034=ORIENTED_EDGE('',*,*,#15215,.F.);
#21035=ORIENTED_EDGE('',*,*,#15210,.F.);
#21036=ORIENTED_EDGE('',*,*,#15181,.T.);
#21037=ORIENTED_EDGE('',*,*,#15184,.T.);
#21038=ORIENTED_EDGE('',*,*,#15187,.T.);
#21039=ORIENTED_EDGE('',*,*,#15190,.T.);
#21040=ORIENTED_EDGE('',*,*,#15193,.T.);
#21041=ORIENTED_EDGE('',*,*,#15196,.T.);
#21042=ORIENTED_EDGE('',*,*,#15199,.T.);
#21043=ORIENTED_EDGE('',*,*,#15209,.F.);
#21044=ORIENTED_EDGE('',*,*,#15223,.F.);
#21045=ORIENTED_EDGE('',*,*,#15224,.T.);
#21046=ORIENTED_EDGE('',*,*,#15200,.T.);
#21047=ORIENTED_EDGE('',*,*,#15224,.F.);
#21048=ORIENTED_EDGE('',*,*,#15225,.F.);
#21049=ORIENTED_EDGE('',*,*,#15203,.T.);
#21050=ORIENTED_EDGE('',*,*,#15221,.T.);
#21051=ORIENTED_EDGE('',*,*,#15218,.F.);
#21052=ORIENTED_EDGE('',*,*,#15226,.F.);
#21053=ORIENTED_EDGE('',*,*,#15227,.T.);
#21054=ORIENTED_EDGE('',*,*,#15222,.T.);
#21055=ORIENTED_EDGE('',*,*,#15227,.F.);
#21056=ORIENTED_EDGE('',*,*,#15228,.F.);
#21057=ORIENTED_EDGE('',*,*,#15213,.T.);
#21058=ORIENTED_EDGE('',*,*,#15214,.T.);
#21059=ORIENTED_EDGE('',*,*,#15228,.T.);
#21060=ORIENTED_EDGE('',*,*,#15226,.T.);
#21061=ORIENTED_EDGE('',*,*,#15217,.T.);
#21062=ORIENTED_EDGE('',*,*,#15204,.T.);
#21063=ORIENTED_EDGE('',*,*,#15225,.T.);
#21064=ORIENTED_EDGE('',*,*,#15223,.T.);
#21065=ORIENTED_EDGE('',*,*,#15208,.T.);
#21066=ORIENTED_EDGE('',*,*,#15183,.F.);
#21067=ORIENTED_EDGE('',*,*,#15186,.F.);
#21068=ORIENTED_EDGE('',*,*,#15189,.F.);
#21069=ORIENTED_EDGE('',*,*,#15192,.F.);
#21070=ORIENTED_EDGE('',*,*,#15195,.F.);
#21071=ORIENTED_EDGE('',*,*,#15198,.F.);
#24089=CYLINDRICAL_SURFACE('',#27682,3.);
#24090=CYLINDRICAL_SURFACE('',#27685,3.);
#24091=CYLINDRICAL_SURFACE('',#27688,3.25);
#24092=CYLINDRICAL_SURFACE('',#27691,3.25);
#24093=CYLINDRICAL_SURFACE('',#27694,3.25);
#24094=CYLINDRICAL_SURFACE('',#27697,3.25);
#25055=ADVANCED_FACE('',(#3102),#24089,.F.);
#25056=ADVANCED_FACE('',(#3103),#24090,.F.);
#25057=ADVANCED_FACE('',(#3104),#24091,.F.);
#25058=ADVANCED_FACE('',(#3105),#24092,.F.);
#25059=ADVANCED_FACE('',(#3106),#24093,.F.);
#25060=ADVANCED_FACE('',(#3107),#24094,.F.);
#25061=ADVANCED_FACE('',(#3108),#2004,.T.);
#25062=ADVANCED_FACE('',(#3109),#2005,.F.);
#25063=ADVANCED_FACE('',(#3110),#2006,.F.);
#25064=ADVANCED_FACE('',(#3111),#2007,.F.);
#25065=ADVANCED_FACE('',(#3112),#2008,.F.);
#25066=ADVANCED_FACE('',(#3113),#2009,.T.);
#25067=ADVANCED_FACE('',(#3114,#1381,#1382,#1383,#1384,#1385,#1386),#2010,
 .F.);
#25068=ADVANCED_FACE('',(#3115),#2011,.F.);
#25069=ADVANCED_FACE('',(#3116),#2012,.F.);
#25070=ADVANCED_FACE('',(#3117),#2013,.F.);
#25071=ADVANCED_FACE('',(#3118),#2014,.F.);
#25072=ADVANCED_FACE('',(#3119,#1387,#1388,#1389,#1390,#1391,#1392),#2015,
 .T.);
#25680=CLOSED_SHELL('',(#25055,#25056,#25057,#25058,#25059,#25060,#25061,
#25062,#25063,#25064,#25065,#25066,#25067,#25068,#25069,#25070,#25071,#25072));
#27681=AXIS2_PLACEMENT_3D('',#41129,#33409,#33410);
#27682=AXIS2_PLACEMENT_3D('',#41130,#33411,#33412);
#27683=AXIS2_PLACEMENT_3D('',#41132,#33413,#33414);
#27684=AXIS2_PLACEMENT_3D('',#41135,#33416,#33417);
#27685=AXIS2_PLACEMENT_3D('',#41136,#33418,#33419);
#27686=AXIS2_PLACEMENT_3D('',#41138,#33420,#33421);
#27687=AXIS2_PLACEMENT_3D('',#41141,#33423,#33424);
#27688=AXIS2_PLACEMENT_3D('',#41142,#33425,#33426);
#27689=AXIS2_PLACEMENT_3D('',#41144,#33427,#33428);
#27690=AXIS2_PLACEMENT_3D('',#41147,#33430,#33431);
#27691=AXIS2_PLACEMENT_3D('',#41148,#33432,#33433);
#27692=AXIS2_PLACEMENT_3D('',#41150,#33434,#33435);
#27693=AXIS2_PLACEMENT_3D('',#41153,#33437,#33438);
#27694=AXIS2_PLACEMENT_3D('',#41154,#33439,#33440);
#27695=AXIS2_PLACEMENT_3D('',#41156,#33441,#33442);
#27696=AXIS2_PLACEMENT_3D('',#41159,#33444,#33445);
#27697=AXIS2_PLACEMENT_3D('',#41160,#33446,#33447);
#27698=AXIS2_PLACEMENT_3D('',#41162,#33448,#33449);
#27699=AXIS2_PLACEMENT_3D('',#41165,#33451,#33452);
#27700=AXIS2_PLACEMENT_3D('',#41166,#33453,#33454);
#27701=AXIS2_PLACEMENT_3D('',#41175,#33459,#33460);
#27702=AXIS2_PLACEMENT_3D('',#41185,#33466,#33467);
#27703=AXIS2_PLACEMENT_3D('',#41193,#33472,#33473);
#27704=AXIS2_PLACEMENT_3D('',#41203,#33479,#33480);
#27705=AXIS2_PLACEMENT_3D('',#41210,#33485,#33486);
#27706=AXIS2_PLACEMENT_3D('',#41214,#33489,#33490);
#27707=AXIS2_PLACEMENT_3D('',#41215,#33491,#33492);
#27708=AXIS2_PLACEMENT_3D('',#41219,#33495,#33496);
#27709=AXIS2_PLACEMENT_3D('',#41221,#33498,#33499);
#27710=AXIS2_PLACEMENT_3D('',#41225,#33502,#33503);
#27711=AXIS2_PLACEMENT_3D('',#41227,#33505,#33506);
#33409=DIRECTION('axis',(0.,0.,1.));
#33410=DIRECTION('refdir',(1.,0.,0.));
#33411=DIRECTION('center_axis',(0.,0.,1.));
#33412=DIRECTION('ref_axis',(1.,0.,0.));
#33413=DIRECTION('center_axis',(0.,0.,1.));
#33414=DIRECTION('ref_axis',(1.,0.,0.));
#33415=DIRECTION('',(0.,0.,1.));
#33416=DIRECTION('center_axis',(0.,0.,1.));
#33417=DIRECTION('ref_axis',(1.,0.,0.));
#33418=DIRECTION('center_axis',(0.,0.,1.));
#33419=DIRECTION('ref_axis',(1.,0.,0.));
#33420=DIRECTION('center_axis',(0.,0.,1.));
#33421=DIRECTION('ref_axis',(1.,0.,0.));
#33422=DIRECTION('',(0.,0.,1.));
#33423=DIRECTION('center_axis',(0.,0.,1.));
#33424=DIRECTION('ref_axis',(1.,0.,0.));
#33425=DIRECTION('center_axis',(0.,0.,1.));
#33426=DIRECTION('ref_axis',(1.,0.,0.));
#33427=DIRECTION('center_axis',(0.,0.,1.));
#33428=DIRECTION('ref_axis',(1.,0.,0.));
#33429=DIRECTION('',(0.,0.,1.));
#33430=DIRECTION('center_axis',(0.,0.,1.));
#33431=DIRECTION('ref_axis',(1.,0.,0.));
#33432=DIRECTION('center_axis',(0.,0.,1.));
#33433=DIRECTION('ref_axis',(1.,0.,0.));
#33434=DIRECTION('center_axis',(0.,0.,1.));
#33435=DIRECTION('ref_axis',(1.,0.,0.));
#33436=DIRECTION('',(0.,0.,1.));
#33437=DIRECTION('center_axis',(0.,0.,1.));
#33438=DIRECTION('ref_axis',(1.,0.,0.));
#33439=DIRECTION('center_axis',(0.,0.,1.));
#33440=DIRECTION('ref_axis',(1.,0.,0.));
#33441=DIRECTION('center_axis',(0.,0.,1.));
#33442=DIRECTION('ref_axis',(1.,0.,0.));
#33443=DIRECTION('',(0.,0.,1.));
#33444=DIRECTION('center_axis',(0.,0.,1.));
#33445=DIRECTION('ref_axis',(1.,0.,0.));
#33446=DIRECTION('center_axis',(0.,0.,1.));
#33447=DIRECTION('ref_axis',(1.,0.,0.));
#33448=DIRECTION('center_axis',(0.,0.,1.));
#33449=DIRECTION('ref_axis',(1.,0.,0.));
#33450=DIRECTION('',(0.,0.,1.));
#33451=DIRECTION('center_axis',(0.,0.,1.));
#33452=DIRECTION('ref_axis',(1.,0.,0.));
#33453=DIRECTION('center_axis',(0.,0.,1.));
#33454=DIRECTION('ref_axis',(1.,0.,0.));
#33455=DIRECTION('',(-3.46944695195362E-16,1.,0.));
#33456=DIRECTION('',(-1.,6.93889390390723E-16,0.));
#33457=DIRECTION('',(-2.31296463463574E-16,1.,0.));
#33458=DIRECTION('',(-1.,0.,0.));
#33459=DIRECTION('center_axis',(-1.,-2.31296463463574E-16,0.));
#33460=DIRECTION('ref_axis',(2.31296463463574E-16,-1.,0.));
#33461=DIRECTION('',(0.,0.,1.));
#33462=DIRECTION('',(-3.46944695195361E-16,1.,0.));
#33463=DIRECTION('',(0.,0.,-1.));
#33464=DIRECTION('',(-2.31296463463574E-16,1.,0.));
#33465=DIRECTION('',(0.,0.,-1.));
#33466=DIRECTION('center_axis',(0.,-1.,0.));
#33467=DIRECTION('ref_axis',(0.,0.,-1.));
#33468=DIRECTION('',(-1.,0.,0.));
#33469=DIRECTION('',(0.,0.,1.));
#33470=DIRECTION('',(-1.,0.,0.));
#33471=DIRECTION('',(0.,0.,-1.));
#33472=DIRECTION('center_axis',(1.,0.,0.));
#33473=DIRECTION('ref_axis',(0.,0.,-1.));
#33474=DIRECTION('',(0.,-1.,0.));
#33475=DIRECTION('',(0.,0.,1.));
#33476=DIRECTION('',(4.95635278850516E-16,-1.,0.));
#33477=DIRECTION('',(0.,-1.,0.));
#33478=DIRECTION('',(0.,0.,-1.));
#33479=DIRECTION('center_axis',(0.,1.,0.));
#33480=DIRECTION('ref_axis',(0.,0.,1.));
#33481=DIRECTION('',(1.,0.,0.));
#33482=DIRECTION('',(0.,0.,1.));
#33483=DIRECTION('',(1.,0.,0.));
#33484=DIRECTION('',(1.,0.,0.));
#33485=DIRECTION('center_axis',(0.,0.,1.));
#33486=DIRECTION('ref_axis',(1.,0.,0.));
#33487=DIRECTION('',(1.73472347597681E-15,-1.,0.));
#33488=DIRECTION('',(1.,6.48494757374508E-17,0.));
#33489=DIRECTION('center_axis',(0.,0.,1.));
#33490=DIRECTION('ref_axis',(1.,0.,0.));
#33491=DIRECTION('center_axis',(1.,3.46944695195362E-16,0.));
#33492=DIRECTION('ref_axis',(-3.46944695195362E-16,1.,0.));
#33493=DIRECTION('',(-3.46944695195362E-16,1.,0.));
#33494=DIRECTION('',(0.,0.,1.));
#33495=DIRECTION('center_axis',(6.93889390390723E-16,1.,0.));
#33496=DIRECTION('ref_axis',(-1.,6.93889390390723E-16,0.));
#33497=DIRECTION('',(-1.,6.93889390390723E-16,0.));
#33498=DIRECTION('center_axis',(-1.,-1.73472347597681E-15,0.));
#33499=DIRECTION('ref_axis',(1.73472347597681E-15,-1.,0.));
#33500=DIRECTION('',(1.73472347597681E-15,-1.,0.));
#33501=DIRECTION('',(0.,0.,1.));
#33502=DIRECTION('center_axis',(6.48494757374508E-17,-1.,0.));
#33503=DIRECTION('ref_axis',(1.,6.48494757374508E-17,0.));
#33504=DIRECTION('',(1.,6.48494757374508E-17,0.));
#33505=DIRECTION('center_axis',(0.,0.,1.));
#33506=DIRECTION('ref_axis',(1.,0.,0.));
#41129=CARTESIAN_POINT('',(0.,0.,0.));
#41130=CARTESIAN_POINT('Origin',(-24.,0.999999999999997,1.5));
#41131=CARTESIAN_POINT('',(-27.,0.999999999999996,-3.5));
#41132=CARTESIAN_POINT('Origin',(-24.,0.999999999999997,-3.5));
#41133=CARTESIAN_POINT('',(-27.,0.999999999999996,1.5));
#41134=CARTESIAN_POINT('',(-27.,0.999999999999996,1.5));
#41135=CARTESIAN_POINT('Origin',(-24.,0.999999999999997,1.5));
#41136=CARTESIAN_POINT('Origin',(0.,-14.,1.5));
#41137=CARTESIAN_POINT('',(-3.,-14.,-3.5));
#41138=CARTESIAN_POINT('Origin',(0.,-14.,-3.5));
#41139=CARTESIAN_POINT('',(-3.,-14.,1.5));
#41140=CARTESIAN_POINT('',(-3.,-14.,1.5));
#41141=CARTESIAN_POINT('Origin',(0.,-14.,1.5));
#41142=CARTESIAN_POINT('Origin',(15.,-14.,-3.5));
#41143=CARTESIAN_POINT('',(11.75,-14.,-3.5));
#41144=CARTESIAN_POINT('Origin',(15.,-14.,-3.5));
#41145=CARTESIAN_POINT('',(11.75,-14.,1.5));
#41146=CARTESIAN_POINT('',(11.75,-14.,-3.5));
#41147=CARTESIAN_POINT('Origin',(15.,-14.,1.5));
#41148=CARTESIAN_POINT('Origin',(-39.,0.999999999999997,-3.5));
#41149=CARTESIAN_POINT('',(-42.25,0.999999999999996,-3.5));
#41150=CARTESIAN_POINT('Origin',(-39.,0.999999999999997,-3.5));
#41151=CARTESIAN_POINT('',(-42.25,0.999999999999996,1.5));
#41152=CARTESIAN_POINT('',(-42.25,0.999999999999996,-3.5));
#41153=CARTESIAN_POINT('Origin',(-39.,0.999999999999997,1.5));
#41154=CARTESIAN_POINT('Origin',(15.,0.999999999999997,-3.5));
#41155=CARTESIAN_POINT('',(11.75,0.999999999999996,-3.5));
#41156=CARTESIAN_POINT('Origin',(15.,0.999999999999997,-3.5));
#41157=CARTESIAN_POINT('',(11.75,0.999999999999996,1.5));
#41158=CARTESIAN_POINT('',(11.75,0.999999999999996,-3.5));
#41159=CARTESIAN_POINT('Origin',(15.,0.999999999999997,1.5));
#41160=CARTESIAN_POINT('Origin',(-39.,-14.,-3.5));
#41161=CARTESIAN_POINT('',(-42.25,-14.,-3.5));
#41162=CARTESIAN_POINT('Origin',(-39.,-14.,-3.5));
#41163=CARTESIAN_POINT('',(-42.25,-14.,1.5));
#41164=CARTESIAN_POINT('',(-42.25,-14.,-3.5));
#41165=CARTESIAN_POINT('Origin',(-39.,-14.,1.5));
#41166=CARTESIAN_POINT('Origin',(0.,0.,3.5));
#41167=CARTESIAN_POINT('',(23.,-12.,3.5));
#41168=CARTESIAN_POINT('',(23.,8.,3.5));
#41169=CARTESIAN_POINT('',(23.,8.,3.5));
#41170=CARTESIAN_POINT('',(25.5,-12.,3.5));
#41171=CARTESIAN_POINT('',(23.,-12.,3.5));
#41172=CARTESIAN_POINT('',(25.5,8.,3.5));
#41173=CARTESIAN_POINT('',(25.5,8.,3.5));
#41174=CARTESIAN_POINT('',(-48.,8.,3.5));
#41175=CARTESIAN_POINT('Origin',(25.5,8.,3.5));
#41176=CARTESIAN_POINT('',(25.5,-12.,1.5));
#41177=CARTESIAN_POINT('',(25.5,-12.,1.5));
#41178=CARTESIAN_POINT('',(25.5,-22.,1.5));
#41179=CARTESIAN_POINT('',(25.5,-22.,1.5));
#41180=CARTESIAN_POINT('',(25.5,-22.,-3.5));
#41181=CARTESIAN_POINT('',(25.5,-22.,3.5));
#41182=CARTESIAN_POINT('',(25.5,8.,-3.5));
#41183=CARTESIAN_POINT('',(25.5,8.,-3.5));
#41184=CARTESIAN_POINT('',(25.5,8.,3.5));
#41185=CARTESIAN_POINT('Origin',(-48.,8.,3.5));
#41186=CARTESIAN_POINT('',(23.,8.,1.5));
#41187=CARTESIAN_POINT('',(-48.,8.,1.5));
#41188=CARTESIAN_POINT('',(-48.,8.,1.5));
#41189=CARTESIAN_POINT('',(23.,8.,1.5));
#41190=CARTESIAN_POINT('',(-48.,8.,-3.5));
#41191=CARTESIAN_POINT('',(-48.,8.,-3.5));
#41192=CARTESIAN_POINT('',(-48.,8.,3.5));
#41193=CARTESIAN_POINT('Origin',(-48.,8.,3.5));
#41194=CARTESIAN_POINT('',(-48.,-20.,3.5));
#41195=CARTESIAN_POINT('',(-48.,-22.,3.5));
#41196=CARTESIAN_POINT('',(-48.,8.,3.5));
#41197=CARTESIAN_POINT('',(-48.,-20.,1.5));
#41198=CARTESIAN_POINT('',(-48.,-20.,1.5));
#41199=CARTESIAN_POINT('',(-48.,8.,1.5));
#41200=CARTESIAN_POINT('',(-48.,-22.,-3.5));
#41201=CARTESIAN_POINT('',(-48.,8.,-3.5));
#41202=CARTESIAN_POINT('',(-48.,-22.,3.5));
#41203=CARTESIAN_POINT('Origin',(-48.,-22.,3.5));
#41204=CARTESIAN_POINT('',(5.49999999999999,-22.,1.5));
#41205=CARTESIAN_POINT('',(5.49999999999999,-22.,1.5));
#41206=CARTESIAN_POINT('',(5.49999999999999,-22.,3.5));
#41207=CARTESIAN_POINT('',(5.49999999999999,-22.,1.5));
#41208=CARTESIAN_POINT('',(-48.,-22.,3.5));
#41209=CARTESIAN_POINT('',(-48.,-22.,-3.5));
#41210=CARTESIAN_POINT('Origin',(0.,0.,3.5));
#41211=CARTESIAN_POINT('',(5.49999999999998,-20.,3.5));
#41212=CARTESIAN_POINT('',(5.49999999999998,-20.,3.5));
#41213=CARTESIAN_POINT('',(-48.,-20.,3.5));
#41214=CARTESIAN_POINT('Origin',(0.,0.,-3.5));
#41215=CARTESIAN_POINT('Origin',(23.,8.,1.5));
#41216=CARTESIAN_POINT('',(23.,-12.,1.5));
#41217=CARTESIAN_POINT('',(23.,8.,1.5));
#41218=CARTESIAN_POINT('',(23.,-12.,1.5));
#41219=CARTESIAN_POINT('Origin',(23.,-12.,1.5));
#41220=CARTESIAN_POINT('',(23.,-12.,1.5));
#41221=CARTESIAN_POINT('Origin',(5.49999999999998,-20.,1.5));
#41222=CARTESIAN_POINT('',(5.49999999999998,-20.,1.5));
#41223=CARTESIAN_POINT('',(5.49999999999998,-20.,1.5));
#41224=CARTESIAN_POINT('',(5.49999999999998,-20.,1.5));
#41225=CARTESIAN_POINT('Origin',(-48.,-20.,1.5));
#41226=CARTESIAN_POINT('',(-48.,-20.,1.5));
#41227=CARTESIAN_POINT('Origin',(0.,0.,1.5));
#66663=UNCERTAINTY_MEASURE_WITH_UNIT(LENGTH_MEASURE(0.01),#66722,
'DISTANCE_ACCURACY_VALUE',
'Maximum model space distance between geometric entities at asserted c
onnectivities');
#66680=UNCERTAINTY_MEASURE_WITH_UNIT(LENGTH_MEASURE(0.01),#66722,
'DISTANCE_ACCURACY_VALUE',
'Maximum model space distance between geometric entities at asserted c
onnectivities');
#66704=(
GEOMETRIC_REPRESENTATION_CONTEXT(3)
GLOBAL_UNCERTAINTY_ASSIGNED_CONTEXT((#66663))
GLOBAL_UNIT_ASSIGNED_CONTEXT((#66722,#66724,#66725))
REPRESENTATION_CONTEXT('','3D')
);
#66721=(
GEOMETRIC_REPRESENTATION_CONTEXT(3)
GLOBAL_UNCERTAINTY_ASSIGNED_CONTEXT((#66680))
GLOBAL_UNIT_ASSIGNED_CONTEXT((#66722,#66724,#66725))
REPRESENTATION_CONTEXT('','3D')
);
#66722=(
LENGTH_UNIT()
NAMED_UNIT(*)
SI_UNIT(.MILLI.,.METRE.)
);
#66724=(
NAMED_UNIT(*)
PLANE_ANGLE_UNIT()
SI_UNIT($,.RADIAN.)
);
#66725=(
NAMED_UNIT(*)
SI_UNIT($,.STERADIAN.)
SOLID_ANGLE_UNIT()
);
#66749=SHAPE_DEFINITION_REPRESENTATION(#66809,#66913);
#66809=PRODUCT_DEFINITION_SHAPE('',$,#66954);
#66913=SHAPE_REPRESENTATION('',(#27681),#66704);
#66930=PRODUCT_DEFINITION_CONTEXT('part definition',#67052,'design');
#66954=PRODUCT_DEFINITION('Ball Screw Spacer 1','Ball Screw Spacer 1',#66994,
#66930);
#66994=PRODUCT_DEFINITION_FORMATION('',$,#67077);
#67052=APPLICATION_CONTEXT(
'Core Data for Automotive Mechanical Design Process');
#67053=PRODUCT_CONTEXT('part definition',#67052,'mechanical');
#67077=PRODUCT('Ball Screw Spacer 1','Ball Screw Spacer 1',$,(#67053));
#67095=PRESENTATION_STYLE_ASSIGNMENT((#67097));
#67097=SURFACE_STYLE_USAGE(.BOTH.,#67099);
#67099=SURFACE_SIDE_STYLE('',(#67101));
#67101=SURFACE_STYLE_FILL_AREA(#67103);
#67103=FILL_AREA_STYLE('Opaque(202,209,238)',(#67105));
#67105=FILL_AREA_STYLE_COLOUR('Opaque(202,209,238)',#67107);
#67107=COLOUR_RGB('Opaque(202,209,238)',0.792156862745098,0.819607843137255,
0.933333333333333);
ENDSEC;
END-ISO-10303-21;
